ISO-10303-21;
HEADER;
/* Generated by software containing ST-Developer
 * from STEP Tools, Inc. (www.steptools.com) 
 */

FILE_DESCRIPTION(
/* description */ (''),
/* implementation_level */ '2;1');

FILE_NAME(
/* name */ 'Guide_Rail_01.step',
/* time_stamp */ '2026-10-19T02:00:06+06:00',
/* author */ (''),
/* organization */ (''),
/* preprocessor_version */ 'ST-DEVELOPER v20.2',
/* originating_system */ 'Autodesk Translation Framework v15.15.0.0',
/* authorisation */ '');

FILE_SCHEMA (('AUTOMOTIVE_DESIGN { 1 0 10303 214 3 1 1 }'));
ENDSEC;

DATA;
#10=MECHANICAL_DESIGN_GEOMETRIC_PRESENTATION_REPRESENTATION('',(#105),#4833);
#83=SHAPE_REPRESENTATION_RELATIONSHIP('SRR','None',#4874,#94);
#94=ADVANCED_BREP_SHAPE_REPRESENTATION('',(#116),#4822);
#105=STYLED_ITEM('',(#5006),#116);
#116=MANIFOLD_SOLID_BREP('Guide_Rail_01',#2687);
#127=FACE_BOUND('',#446,.T.);
#128=FACE_BOUND('',#447,.T.);
#129=FACE_BOUND('',#448,.T.);
#130=FACE_BOUND('',#449,.T.);
#131=FACE_BOUND('',#450,.T.);
#132=FACE_BOUND('',#451,.T.);
#164=PLANE('',#2825);
#165=PLANE('',#2829);
#166=PLANE('',#2833);
#167=PLANE('',#2837);
#168=PLANE('',#2841);
#169=PLANE('',#2845);
#170=PLANE('',#2846);
#171=PLANE('',#2847);
#172=PLANE('',#2848);
#173=PLANE('',#2849);
#174=PLANE('',#2850);
#175=PLANE('',#2851);
#268=FACE_OUTER_BOUND('',#429,.T.);
#269=FACE_OUTER_BOUND('',#430,.T.);
#270=FACE_OUTER_BOUND('',#431,.T.);
#271=FACE_OUTER_BOUND('',#432,.T.);
#272=FACE_OUTER_BOUND('',#433,.T.);
#273=FACE_OUTER_BOUND('',#434,.T.);
#274=FACE_OUTER_BOUND('',#435,.T.);
#275=FACE_OUTER_BOUND('',#436,.T.);
#276=FACE_OUTER_BOUND('',#437,.T.);
#277=FACE_OUTER_BOUND('',#438,.T.);
#278=FACE_OUTER_BOUND('',#439,.T.);
#279=FACE_OUTER_BOUND('',#440,.T.);
#280=FACE_OUTER_BOUND('',#441,.T.);
#281=FACE_OUTER_BOUND('',#442,.T.);
#282=FACE_OUTER_BOUND('',#443,.T.);
#283=FACE_OUTER_BOUND('',#444,.T.);
#284=FACE_OUTER_BOUND('',#445,.T.);
#285=FACE_OUTER_BOUND('',#452,.T.);
#429=EDGE_LOOP('',(#1777,#1778,#1779,#1780));
#430=EDGE_LOOP('',(#1781));
#431=EDGE_LOOP('',(#1782,#1783,#1784,#1785));
#432=EDGE_LOOP('',(#1786));
#433=EDGE_LOOP('',(#1787,#1788,#1789,#1790));
#434=EDGE_LOOP('',(#1791));
#435=EDGE_LOOP('',(#1792,#1793,#1794,#1795));
#436=EDGE_LOOP('',(#1796));
#437=EDGE_LOOP('',(#1797,#1798,#1799,#1800));
#438=EDGE_LOOP('',(#1801));
#439=EDGE_LOOP('',(#1802,#1803,#1804,#1805));
#440=EDGE_LOOP('',(#1806));
#441=EDGE_LOOP('',(#1807,#1808,#1809,#1810));
#442=EDGE_LOOP('',(#1811,#1812,#1813,#1814));
#443=EDGE_LOOP('',(#1815,#1816,#1817,#1818));
#444=EDGE_LOOP('',(#1819,#1820,#1821,#1822));
#445=EDGE_LOOP('',(#1823,#1824,#1825,#1826));
#446=EDGE_LOOP('',(#1827));
#447=EDGE_LOOP('',(#1828));
#448=EDGE_LOOP('',(#1829));
#449=EDGE_LOOP('',(#1830));
#450=EDGE_LOOP('',(#1831));
#451=EDGE_LOOP('',(#1832));
#452=EDGE_LOOP('',(#1833,#1834,#1835,#1836));
#627=LINE('',#3890,#881);
#628=LINE('',#3897,#882);
#629=LINE('',#3904,#883);
#630=LINE('',#3911,#884);
#631=LINE('',#3918,#885);
#632=LINE('',#3925,#886);
#633=LINE('',#3931,#887);
#634=LINE('',#3933,#888);
#635=LINE('',#3935,#889);
#636=LINE('',#3936,#890);
#637=LINE('',#3939,#891);
#638=LINE('',#3941,#892);
#639=LINE('',#3942,#893);
#640=LINE('',#3945,#894);
#641=LINE('',#3947,#895);
#642=LINE('',#3948,#896);
#643=LINE('',#3950,#897);
#644=LINE('',#3951,#898);
#881=VECTOR('',#3098,4.);
#882=VECTOR('',#3107,4.);
#883=VECTOR('',#3116,4.);
#884=VECTOR('',#3125,4.);
#885=VECTOR('',#3134,4.);
#886=VECTOR('',#3143,4.);
#887=VECTOR('',#3150,10.);
#888=VECTOR('',#3151,10.);
#889=VECTOR('',#3152,10.);
#890=VECTOR('',#3153,10.);
#891=VECTOR('',#3156,10.);
#892=VECTOR('',#3157,10.);
#893=VECTOR('',#3158,10.);
#894=VECTOR('',#3161,10.);
#895=VECTOR('',#3162,10.);
#896=VECTOR('',#3163,10.);
#897=VECTOR('',#3166,10.);
#898=VECTOR('',#3167,10.);
#1135=CIRCLE('',#2823,4.);
#1136=CIRCLE('',#2824,4.);
#1137=CIRCLE('',#2827,4.);
#1138=CIRCLE('',#2828,4.);
#1139=CIRCLE('',#2831,4.);
#1140=CIRCLE('',#2832,4.);
#1141=CIRCLE('',#2835,4.);
#1142=CIRCLE('',#2836,4.);
#1143=CIRCLE('',#2839,4.);
#1144=CIRCLE('',#2840,4.);
#1145=CIRCLE('',#2843,4.);
#1146=CIRCLE('',#2844,4.);
#1205=VERTEX_POINT('',#3887);
#1206=VERTEX_POINT('',#3889);
#1207=VERTEX_POINT('',#3894);
#1208=VERTEX_POINT('',#3896);
#1209=VERTEX_POINT('',#3901);
#1210=VERTEX_POINT('',#3903);
#1211=VERTEX_POINT('',#3908);
#1212=VERTEX_POINT('',#3910);
#1213=VERTEX_POINT('',#3915);
#1214=VERTEX_POINT('',#3917);
#1215=VERTEX_POINT('',#3922);
#1216=VERTEX_POINT('',#3924);
#1217=VERTEX_POINT('',#3929);
#1218=VERTEX_POINT('',#3930);
#1219=VERTEX_POINT('',#3932);
#1220=VERTEX_POINT('',#3934);
#1221=VERTEX_POINT('',#3938);
#1222=VERTEX_POINT('',#3940);
#1223=VERTEX_POINT('',#3944);
#1224=VERTEX_POINT('',#3946);
#1429=EDGE_CURVE('',#1205,#1205,#1135,.T.);
#1430=EDGE_CURVE('',#1205,#1206,#627,.T.);
#1431=EDGE_CURVE('',#1206,#1206,#1136,.T.);
#1432=EDGE_CURVE('',#1207,#1207,#1137,.T.);
#1433=EDGE_CURVE('',#1207,#1208,#628,.T.);
#1434=EDGE_CURVE('',#1208,#1208,#1138,.T.);
#1435=EDGE_CURVE('',#1209,#1209,#1139,.T.);
#1436=EDGE_CURVE('',#1209,#1210,#629,.T.);
#1437=EDGE_CURVE('',#1210,#1210,#1140,.T.);
#1438=EDGE_CURVE('',#1211,#1211,#1141,.T.);
#1439=EDGE_CURVE('',#1211,#1212,#630,.T.);
#1440=EDGE_CURVE('',#1212,#1212,#1142,.T.);
#1441=EDGE_CURVE('',#1213,#1213,#1143,.T.);
#1442=EDGE_CURVE('',#1213,#1214,#631,.T.);
#1443=EDGE_CURVE('',#1214,#1214,#1144,.T.);
#1444=EDGE_CURVE('',#1215,#1215,#1145,.T.);
#1445=EDGE_CURVE('',#1215,#1216,#632,.T.);
#1446=EDGE_CURVE('',#1216,#1216,#1146,.T.);
#1447=EDGE_CURVE('',#1217,#1218,#633,.T.);
#1448=EDGE_CURVE('',#1218,#1219,#634,.T.);
#1449=EDGE_CURVE('',#1220,#1219,#635,.T.);
#1450=EDGE_CURVE('',#1217,#1220,#636,.T.);
#1451=EDGE_CURVE('',#1221,#1217,#637,.T.);
#1452=EDGE_CURVE('',#1222,#1220,#638,.T.);
#1453=EDGE_CURVE('',#1221,#1222,#639,.T.);
#1454=EDGE_CURVE('',#1223,#1221,#640,.T.);
#1455=EDGE_CURVE('',#1224,#1222,#641,.T.);
#1456=EDGE_CURVE('',#1223,#1224,#642,.T.);
#1457=EDGE_CURVE('',#1218,#1223,#643,.T.);
#1458=EDGE_CURVE('',#1219,#1224,#644,.T.);
#1777=ORIENTED_EDGE('',*,*,#1429,.F.);
#1778=ORIENTED_EDGE('',*,*,#1430,.T.);
#1779=ORIENTED_EDGE('',*,*,#1431,.T.);
#1780=ORIENTED_EDGE('',*,*,#1430,.F.);
#1781=ORIENTED_EDGE('',*,*,#1431,.F.);
#1782=ORIENTED_EDGE('',*,*,#1432,.F.);
#1783=ORIENTED_EDGE('',*,*,#1433,.T.);
#1784=ORIENTED_EDGE('',*,*,#1434,.T.);
#1785=ORIENTED_EDGE('',*,*,#1433,.F.);
#1786=ORIENTED_EDGE('',*,*,#1434,.F.);
#1787=ORIENTED_EDGE('',*,*,#1435,.F.);
#1788=ORIENTED_EDGE('',*,*,#1436,.T.);
#1789=ORIENTED_EDGE('',*,*,#1437,.T.);
#1790=ORIENTED_EDGE('',*,*,#1436,.F.);
#1791=ORIENTED_EDGE('',*,*,#1437,.F.);
#1792=ORIENTED_EDGE('',*,*,#1438,.F.);
#1793=ORIENTED_EDGE('',*,*,#1439,.T.);
#1794=ORIENTED_EDGE('',*,*,#1440,.T.);
#1795=ORIENTED_EDGE('',*,*,#1439,.F.);
#1796=ORIENTED_EDGE('',*,*,#1440,.F.);
#1797=ORIENTED_EDGE('',*,*,#1441,.F.);
#1798=ORIENTED_EDGE('',*,*,#1442,.T.);
#1799=ORIENTED_EDGE('',*,*,#1443,.T.);
#1800=ORIENTED_EDGE('',*,*,#1442,.F.);
#1801=ORIENTED_EDGE('',*,*,#1443,.F.);
#1802=ORIENTED_EDGE('',*,*,#1444,.F.);
#1803=ORIENTED_EDGE('',*,*,#1445,.T.);
#1804=ORIENTED_EDGE('',*,*,#1446,.T.);
#1805=ORIENTED_EDGE('',*,*,#1445,.F.);
#1806=ORIENTED_EDGE('',*,*,#1446,.F.);
#1807=ORIENTED_EDGE('',*,*,#1447,.T.);
#1808=ORIENTED_EDGE('',*,*,#1448,.T.);
#1809=ORIENTED_EDGE('',*,*,#1449,.F.);
#1810=ORIENTED_EDGE('',*,*,#1450,.F.);
#1811=ORIENTED_EDGE('',*,*,#1451,.T.);
#1812=ORIENTED_EDGE('',*,*,#1450,.T.);
#1813=ORIENTED_EDGE('',*,*,#1452,.F.);
#1814=ORIENTED_EDGE('',*,*,#1453,.F.);
#1815=ORIENTED_EDGE('',*,*,#1454,.T.);
#1816=ORIENTED_EDGE('',*,*,#1453,.T.);
#1817=ORIENTED_EDGE('',*,*,#1455,.F.);
#1818=ORIENTED_EDGE('',*,*,#1456,.F.);
#1819=ORIENTED_EDGE('',*,*,#1457,.T.);
#1820=ORIENTED_EDGE('',*,*,#1456,.T.);
#1821=ORIENTED_EDGE('',*,*,#1458,.F.);
#1822=ORIENTED_EDGE('',*,*,#1448,.F.);
#1823=ORIENTED_EDGE('',*,*,#1458,.T.);
#1824=ORIENTED_EDGE('',*,*,#1455,.T.);
#1825=ORIENTED_EDGE('',*,*,#1452,.T.);
#1826=ORIENTED_EDGE('',*,*,#1449,.T.);
#1827=ORIENTED_EDGE('',*,*,#1444,.T.);
#1828=ORIENTED_EDGE('',*,*,#1441,.T.);
#1829=ORIENTED_EDGE('',*,*,#1438,.T.);
#1830=ORIENTED_EDGE('',*,*,#1435,.T.);
#1831=ORIENTED_EDGE('',*,*,#1432,.T.);
#1832=ORIENTED_EDGE('',*,*,#1429,.T.);
#1833=ORIENTED_EDGE('',*,*,#1457,.F.);
#1834=ORIENTED_EDGE('',*,*,#1447,.F.);
#1835=ORIENTED_EDGE('',*,*,#1451,.F.);
#1836=ORIENTED_EDGE('',*,*,#1454,.F.);
#2473=CYLINDRICAL_SURFACE('',#2822,4.);
#2474=CYLINDRICAL_SURFACE('',#2826,4.);
#2475=CYLINDRICAL_SURFACE('',#2830,4.);
#2476=CYLINDRICAL_SURFACE('',#2834,4.);
#2477=CYLINDRICAL_SURFACE('',#2838,4.);
#2478=CYLINDRICAL_SURFACE('',#2842,4.);
#2526=ADVANCED_FACE('',(#268),#2473,.F.);
#2527=ADVANCED_FACE('',(#269),#164,.T.);
#2528=ADVANCED_FACE('',(#270),#2474,.F.);
#2529=ADVANCED_FACE('',(#271),#165,.T.);
#2530=ADVANCED_FACE('',(#272),#2475,.F.);
#2531=ADVANCED_FACE('',(#273),#166,.T.);
#2532=ADVANCED_FACE('',(#274),#2476,.F.);
#2533=ADVANCED_FACE('',(#275),#167,.T.);
#2534=ADVANCED_FACE('',(#276),#2477,.F.);
#2535=ADVANCED_FACE('',(#277),#168,.T.);
#2536=ADVANCED_FACE('',(#278),#2478,.F.);
#2537=ADVANCED_FACE('',(#279),#169,.T.);
#2538=ADVANCED_FACE('',(#280),#170,.T.);
#2539=ADVANCED_FACE('',(#281),#171,.T.);
#2540=ADVANCED_FACE('',(#282),#172,.T.);
#2541=ADVANCED_FACE('',(#283),#173,.T.);
#2542=ADVANCED_FACE('',(#284,#127,#128,#129,#130,#131,#132),#174,.T.);
#2543=ADVANCED_FACE('',(#285),#175,.F.);
#2687=CLOSED_SHELL('',(#2526,#2527,#2528,#2529,#2530,#2531,#2532,#2533,
#2534,#2535,#2536,#2537,#2538,#2539,#2540,#2541,#2542,#2543));
#2821=AXIS2_PLACEMENT_3D('',#3885,#3092,#3093);
#2822=AXIS2_PLACEMENT_3D('',#3886,#3094,#3095);
#2823=AXIS2_PLACEMENT_3D('',#3888,#3096,#3097);
#2824=AXIS2_PLACEMENT_3D('',#3891,#3099,#3100);
#2825=AXIS2_PLACEMENT_3D('',#3892,#3101,#3102);
#2826=AXIS2_PLACEMENT_3D('',#3893,#3103,#3104);
#2827=AXIS2_PLACEMENT_3D('',#3895,#3105,#3106);
#2828=AXIS2_PLACEMENT_3D('',#3898,#3108,#3109);
#2829=AXIS2_PLACEMENT_3D('',#3899,#3110,#3111);
#2830=AXIS2_PLACEMENT_3D('',#3900,#3112,#3113);
#2831=AXIS2_PLACEMENT_3D('',#3902,#3114,#3115);
#2832=AXIS2_PLACEMENT_3D('',#3905,#3117,#3118);
#2833=AXIS2_PLACEMENT_3D('',#3906,#3119,#3120);
#2834=AXIS2_PLACEMENT_3D('',#3907,#3121,#3122);
#2835=AXIS2_PLACEMENT_3D('',#3909,#3123,#3124);
#2836=AXIS2_PLACEMENT_3D('',#3912,#3126,#3127);
#2837=AXIS2_PLACEMENT_3D('',#3913,#3128,#3129);
#2838=AXIS2_PLACEMENT_3D('',#3914,#3130,#3131);
#2839=AXIS2_PLACEMENT_3D('',#3916,#3132,#3133);
#2840=AXIS2_PLACEMENT_3D('',#3919,#3135,#3136);
#2841=AXIS2_PLACEMENT_3D('',#3920,#3137,#3138);
#2842=AXIS2_PLACEMENT_3D('',#3921,#3139,#3140);
#2843=AXIS2_PLACEMENT_3D('',#3923,#3141,#3142);
#2844=AXIS2_PLACEMENT_3D('',#3926,#3144,#3145);
#2845=AXIS2_PLACEMENT_3D('',#3927,#3146,#3147);
#2846=AXIS2_PLACEMENT_3D('',#3928,#3148,#3149);
#2847=AXIS2_PLACEMENT_3D('',#3937,#3154,#3155);
#2848=AXIS2_PLACEMENT_3D('',#3943,#3159,#3160);
#2849=AXIS2_PLACEMENT_3D('',#3949,#3164,#3165);
#2850=AXIS2_PLACEMENT_3D('',#3952,#3168,#3169);
#2851=AXIS2_PLACEMENT_3D('',#3953,#3170,#3171);
#3092=DIRECTION('axis',(0.,0.,1.));
#3093=DIRECTION('refdir',(1.,0.,0.));
#3094=DIRECTION('center_axis',(0.,0.,-1.));
#3095=DIRECTION('ref_axis',(-1.,0.,0.));
#3096=DIRECTION('center_axis',(0.,0.,-1.));
#3097=DIRECTION('ref_axis',(-1.,0.,0.));
#3098=DIRECTION('',(0.,0.,-1.));
#3099=DIRECTION('center_axis',(0.,0.,-1.));
#3100=DIRECTION('ref_axis',(-1.,0.,0.));
#3101=DIRECTION('center_axis',(0.,0.,1.));
#3102=DIRECTION('ref_axis',(-1.,0.,0.));
#3103=DIRECTION('center_axis',(0.,0.,-1.));
#3104=DIRECTION('ref_axis',(-1.,0.,0.));
#3105=DIRECTION('center_axis',(0.,0.,-1.));
#3106=DIRECTION('ref_axis',(-1.,0.,0.));
#3107=DIRECTION('',(0.,0.,-1.));
#3108=DIRECTION('center_axis',(0.,0.,-1.));
#3109=DIRECTION('ref_axis',(-1.,0.,0.));
#3110=DIRECTION('center_axis',(0.,0.,1.));
#3111=DIRECTION('ref_axis',(-1.,0.,0.));
#3112=DIRECTION('center_axis',(0.,0.,-1.));
#3113=DIRECTION('ref_axis',(-1.,0.,0.));
#3114=DIRECTION('center_axis',(0.,0.,-1.));
#3115=DIRECTION('ref_axis',(-1.,0.,0.));
#3116=DIRECTION('',(0.,0.,-1.));
#3117=DIRECTION('center_axis',(0.,0.,-1.));
#3118=DIRECTION('ref_axis',(-1.,0.,0.));
#3119=DIRECTION('center_axis',(0.,0.,1.));
#3120=DIRECTION('ref_axis',(-1.,0.,0.));
#3121=DIRECTION('center_axis',(0.,0.,-1.));
#3122=DIRECTION('ref_axis',(-1.,0.,0.));
#3123=DIRECTION('center_axis',(0.,0.,-1.));
#3124=DIRECTION('ref_axis',(-1.,0.,0.));
#3125=DIRECTION('',(0.,0.,-1.));
#3126=DIRECTION('center_axis',(0.,0.,-1.));
#3127=DIRECTION('ref_axis',(-1.,0.,0.));
#3128=DIRECTION('center_axis',(0.,0.,1.));
#3129=DIRECTION('ref_axis',(-1.,0.,0.));
#3130=DIRECTION('center_axis',(0.,0.,-1.));
#3131=DIRECTION('ref_axis',(-1.,0.,0.));
#3132=DIRECTION('center_axis',(0.,0.,-1.));
#3133=DIRECTION('ref_axis',(-1.,0.,0.));
#3134=DIRECTION('',(0.,0.,-1.));
#3135=DIRECTION('center_axis',(0.,0.,-1.));
#3136=DIRECTION('ref_axis',(-1.,0.,0.));
#3137=DIRECTION('center_axis',(0.,0.,1.));
#3138=DIRECTION('ref_axis',(-1.,0.,0.));
#3139=DIRECTION('center_axis',(0.,0.,-1.));
#3140=DIRECTION('ref_axis',(-1.,0.,0.));
#3141=DIRECTION('center_axis',(0.,0.,-1.));
#3142=DIRECTION('ref_axis',(-1.,0.,0.));
#3143=DIRECTION('',(0.,0.,-1.));
#3144=DIRECTION('center_axis',(0.,0.,-1.));
#3145=DIRECTION('ref_axis',(-1.,0.,0.));
#3146=DIRECTION('center_axis',(0.,0.,1.));
#3147=DIRECTION('ref_axis',(-1.,0.,0.));
#3148=DIRECTION('center_axis',(1.,0.,0.));
#3149=DIRECTION('ref_axis',(0.,1.,0.));
#3150=DIRECTION('',(0.,1.,0.));
#3151=DIRECTION('',(0.,0.,1.));
#3152=DIRECTION('',(0.,1.,0.));
#3153=DIRECTION('',(0.,0.,1.));
#3154=DIRECTION('center_axis',(0.,-1.,0.));
#3155=DIRECTION('ref_axis',(1.,0.,0.));
#3156=DIRECTION('',(1.,0.,0.));
#3157=DIRECTION('',(1.,0.,0.));
#3158=DIRECTION('',(0.,0.,1.));
#3159=DIRECTION('center_axis',(-1.,0.,0.));
#3160=DIRECTION('ref_axis',(0.,-1.,0.));
#3161=DIRECTION('',(0.,-1.,0.));
#3162=DIRECTION('',(0.,-1.,0.));
#3163=DIRECTION('',(0.,0.,1.));
#3164=DIRECTION('center_axis',(0.,1.,0.));
#3165=DIRECTION('ref_axis',(-1.,0.,0.));
#3166=DIRECTION('',(-1.,0.,0.));
#3167=DIRECTION('',(-1.,0.,0.));
#3168=DIRECTION('center_axis',(0.,0.,1.));
#3169=DIRECTION('ref_axis',(1.,0.,0.));
#3170=DIRECTION('center_axis',(0.,0.,1.));
#3171=DIRECTION('ref_axis',(-1.,0.,0.));
#3885=CARTESIAN_POINT('',(0.,0.,0.));
#3886=CARTESIAN_POINT('Origin',(-22.,-75.0000000000105,14.0000000000021));
#3887=CARTESIAN_POINT('',(-18.,-75.0000000000105,14.0000000000021));
#3888=CARTESIAN_POINT('Origin',(-22.,-75.0000000000105,14.0000000000021));
#3889=CARTESIAN_POINT('',(-18.,-75.0000000000105,8.00000000000211));
#3890=CARTESIAN_POINT('',(-18.,-75.0000000000105,14.0000000000021));
#3891=CARTESIAN_POINT('Origin',(-22.,-75.0000000000105,8.00000000000211));
#3892=CARTESIAN_POINT('Origin',(-22.,-75.0000000000105,8.00000000000211));
#3893=CARTESIAN_POINT('Origin',(56.,-75.0000000000105,14.0000000000021));
#3894=CARTESIAN_POINT('',(60.,-75.0000000000105,14.0000000000021));
#3895=CARTESIAN_POINT('Origin',(56.,-75.0000000000105,14.0000000000021));
#3896=CARTESIAN_POINT('',(60.,-75.0000000000105,8.00000000000211));
#3897=CARTESIAN_POINT('',(60.,-75.0000000000105,14.0000000000021));
#3898=CARTESIAN_POINT('Origin',(56.,-75.0000000000105,8.00000000000211));
#3899=CARTESIAN_POINT('Origin',(56.,-75.0000000000105,8.00000000000211));
#3900=CARTESIAN_POINT('Origin',(-48.,-75.0000000000105,14.0000000000021));
#3901=CARTESIAN_POINT('',(-44.,-75.0000000000105,14.0000000000021));
#3902=CARTESIAN_POINT('Origin',(-48.,-75.0000000000105,14.0000000000021));
#3903=CARTESIAN_POINT('',(-44.,-75.0000000000105,8.00000000000211));
#3904=CARTESIAN_POINT('',(-44.,-75.0000000000105,14.0000000000021));
#3905=CARTESIAN_POINT('Origin',(-48.,-75.0000000000105,8.00000000000211));
#3906=CARTESIAN_POINT('Origin',(-48.,-75.0000000000105,8.00000000000211));
#3907=CARTESIAN_POINT('Origin',(4.,-75.0000000000105,14.0000000000021));
#3908=CARTESIAN_POINT('',(8.,-75.0000000000105,14.0000000000021));
#3909=CARTESIAN_POINT('Origin',(4.,-75.0000000000105,14.0000000000021));
#3910=CARTESIAN_POINT('',(8.,-75.0000000000105,8.00000000000211));
#3911=CARTESIAN_POINT('',(8.,-75.0000000000105,14.0000000000021));
#3912=CARTESIAN_POINT('Origin',(4.,-75.0000000000105,8.00000000000211));
#3913=CARTESIAN_POINT('Origin',(4.,-75.0000000000105,8.00000000000211));
#3914=CARTESIAN_POINT('Origin',(30.,-75.0000000000105,14.0000000000021));
#3915=CARTESIAN_POINT('',(34.,-75.0000000000105,14.0000000000021));
#3916=CARTESIAN_POINT('Origin',(30.,-75.0000000000105,14.0000000000021));
#3917=CARTESIAN_POINT('',(34.,-75.0000000000105,8.00000000000211));
#3918=CARTESIAN_POINT('',(34.,-75.0000000000105,14.0000000000021));
#3919=CARTESIAN_POINT('Origin',(30.,-75.0000000000105,8.00000000000211));
#3920=CARTESIAN_POINT('Origin',(30.,-75.0000000000105,8.00000000000211));
#3921=CARTESIAN_POINT('Origin',(-74.,-75.0000000000105,14.0000000000021));
#3922=CARTESIAN_POINT('',(-70.,-75.0000000000105,14.0000000000021));
#3923=CARTESIAN_POINT('Origin',(-74.,-75.0000000000105,14.0000000000021));
#3924=CARTESIAN_POINT('',(-70.,-75.0000000000105,8.00000000000211));
#3925=CARTESIAN_POINT('',(-70.,-75.0000000000105,14.0000000000021));
#3926=CARTESIAN_POINT('Origin',(-74.,-75.0000000000105,8.00000000000211));
#3927=CARTESIAN_POINT('Origin',(-74.,-75.0000000000105,8.00000000000211));
#3928=CARTESIAN_POINT('Origin',(70.,-81.0000000000105,4.00000000000212));
#3929=CARTESIAN_POINT('',(70.,-81.0000000000105,4.00000000000212));
#3930=CARTESIAN_POINT('',(70.,-69.0000000000105,4.00000000000212));
#3931=CARTESIAN_POINT('',(70.,-81.0000000000105,4.00000000000212));
#3932=CARTESIAN_POINT('',(70.,-69.0000000000105,14.0000000000021));
#3933=CARTESIAN_POINT('',(70.,-69.0000000000105,4.00000000000212));
#3934=CARTESIAN_POINT('',(70.,-81.0000000000105,14.0000000000021));
#3935=CARTESIAN_POINT('',(70.,-81.0000000000105,14.0000000000021));
#3936=CARTESIAN_POINT('',(70.,-81.0000000000105,4.00000000000212));
#3937=CARTESIAN_POINT('Origin',(-90.,-81.0000000000105,4.00000000000212));
#3938=CARTESIAN_POINT('',(-90.,-81.0000000000105,4.00000000000212));
#3939=CARTESIAN_POINT('',(-90.,-81.0000000000105,4.00000000000212));
#3940=CARTESIAN_POINT('',(-90.,-81.0000000000105,14.0000000000021));
#3941=CARTESIAN_POINT('',(-90.,-81.0000000000105,14.0000000000021));
#3942=CARTESIAN_POINT('',(-90.,-81.0000000000105,4.00000000000212));
#3943=CARTESIAN_POINT('Origin',(-90.,-69.0000000000105,4.00000000000212));
#3944=CARTESIAN_POINT('',(-90.,-69.0000000000105,4.00000000000212));
#3945=CARTESIAN_POINT('',(-90.,-69.0000000000105,4.00000000000212));
#3946=CARTESIAN_POINT('',(-90.,-69.0000000000105,14.0000000000021));
#3947=CARTESIAN_POINT('',(-90.,-69.0000000000105,14.0000000000021));
#3948=CARTESIAN_POINT('',(-90.,-69.0000000000105,4.00000000000212));
#3949=CARTESIAN_POINT('Origin',(70.,-69.0000000000105,4.00000000000212));
#3950=CARTESIAN_POINT('',(70.,-69.0000000000105,4.00000000000212));
#3951=CARTESIAN_POINT('',(70.,-69.0000000000105,14.0000000000021));
#3952=CARTESIAN_POINT('Origin',(-10.,-75.0000000000105,14.0000000000021));
#3953=CARTESIAN_POINT('Origin',(-10.,-75.0000000000105,4.00000000000212));
#4809=UNCERTAINTY_MEASURE_WITH_UNIT(LENGTH_MEASURE(0.01),#4834,
'DISTANCE_ACCURACY_VALUE',
'Maximum model space distance between geometric entities at asserted c
onnectivities');
#4820=UNCERTAINTY_MEASURE_WITH_UNIT(LENGTH_MEASURE(0.01),#4834,
'DISTANCE_ACCURACY_VALUE',
'Maximum model space distance between geometric entities at asserted c
onnectivities');
#4822=(
GEOMETRIC_REPRESENTATION_CONTEXT(3)
GLOBAL_UNCERTAINTY_ASSIGNED_CONTEXT((#4809))
GLOBAL_UNIT_ASSIGNED_CONTEXT((#4834,#4836,#4837))
REPRESENTATION_CONTEXT('','3D')
);
#4833=(
GEOMETRIC_REPRESENTATION_CONTEXT(3)
GLOBAL_UNCERTAINTY_ASSIGNED_CONTEXT((#4820))
GLOBAL_UNIT_ASSIGNED_CONTEXT((#4834,#4836,#4837))
REPRESENTATION_CONTEXT('','3D')
);
#4834=(
LENGTH_UNIT()
NAMED_UNIT(*)
SI_UNIT(.MILLI.,.METRE.)
);
#4836=(
NAMED_UNIT(*)
PLANE_ANGLE_UNIT()
SI_UNIT($,.RADIAN.)
);
#4837=(
NAMED_UNIT(*)
SI_UNIT($,.STERADIAN.)
SOLID_ANGLE_UNIT()
);
#4839=SHAPE_DEFINITION_REPRESENTATION(#4851,#4874);
#4851=PRODUCT_DEFINITION_SHAPE('',$,#4887);
#4874=SHAPE_REPRESENTATION('',(#2821),#4822);
#4885=PRODUCT_DEFINITION_CONTEXT('part definition',#4923,'design');
#4887=PRODUCT_DEFINITION('Guide_Rail_01','Guide_Rail_01',#4899,#4885);
#4899=PRODUCT_DEFINITION_FORMATION('',$,#4926);
#4923=APPLICATION_CONTEXT(
'Core Data for Automotive Mechanical Design Process');
#4924=PRODUCT_CONTEXT('part definition',#4923,'mechanical');
#4926=PRODUCT('Guide_Rail_01','Guide_Rail_01',$,(#4924));
#5000=COLOUR_RGB('Off White',0.89,0.88,0.83);
#5001=FILL_AREA_STYLE_COLOUR('',#5000);
#5002=FILL_AREA_STYLE('',(#5001));
#5003=SURFACE_STYLE_FILL_AREA(#5002);
#5004=SURFACE_SIDE_STYLE('',(#5003));
#5005=SURFACE_STYLE_USAGE(.BOTH.,#5004);
#5006=PRESENTATION_STYLE_ASSIGNMENT((#5005));
ENDSEC;
END-ISO-10303-21;
